ISO-10303-21;
HEADER;
/* Generated by software containing ST-Developer
 * from STEP Tools, Inc. (www.steptools.com) 
 */

FILE_DESCRIPTION(
/* description */ (''),
/* implementation_level */ '2;1');

FILE_NAME(
/* name */ '09_Impeller_Drive_Pin_D5x23.step',
/* time_stamp */ '2026-10-26T04:15:57-07:00',
/* author */ (''),
/* organization */ (''),
/* preprocessor_version */ 'ST-DEVELOPER v20.2',
/* originating_system */ 'Autodesk Translation Framework v15.15.0.0',
/* authorisation */ '');

FILE_SCHEMA (('AUTOMOTIVE_DESIGN { 1 0 10303 214 3 1 1 }'));
ENDSEC;

DATA;
#10=MECHANICAL_DESIGN_GEOMETRIC_PRESENTATION_REPRESENTATION('',(#460),#55737);
#377=CONICAL_SURFACE('',#29180,2.35,0.785398163397447);
#378=CONICAL_SURFACE('',#29184,2.35,0.785398163397447);
#420=SHAPE_REPRESENTATION_RELATIONSHIP('SRR','None',#55829,#440);
#440=ADVANCED_BREP_SHAPE_REPRESENTATION('',(#480),#55725);
#460=STYLED_ITEM('',(#55991),#480);
#480=MANIFOLD_SOLID_BREP('Body1',#27229);
#1393=PLANE('',#29178);
#1394=PLANE('',#29186);
#3335=LINE('',#45249,#5706);
#3336=LINE('',#45253,#5707);
#3337=LINE('',#45257,#5708);
#5706=VECTOR('',#34993,2.35);
#5707=VECTOR('',#34998,2.5);
#5708=VECTOR('',#35003,2.35);
#6691=CYLINDRICAL_SURFACE('',#29182,2.5);
#7846=FACE_OUTER_BOUND('',#9513,.T.);
#7847=FACE_OUTER_BOUND('',#9514,.T.);
#7848=FACE_OUTER_BOUND('',#9515,.T.);
#7849=FACE_OUTER_BOUND('',#9516,.T.);
#7850=FACE_OUTER_BOUND('',#9517,.T.);
#9513=EDGE_LOOP('',(#22976));
#9514=EDGE_LOOP('',(#22977,#22978,#22979,#22980));
#9515=EDGE_LOOP('',(#22981,#22982,#22983,#22984));
#9516=EDGE_LOOP('',(#22985,#22986,#22987,#22988));
#9517=EDGE_LOOP('',(#22989));
#10772=CIRCLE('',#29179,2.2);
#10773=CIRCLE('',#29181,2.5);
#10774=CIRCLE('',#29183,2.5);
#10775=CIRCLE('',#29185,2.2);
#13083=VERTEX_POINT('',#45244);
#13084=VERTEX_POINT('',#45247);
#13085=VERTEX_POINT('',#45251);
#13086=VERTEX_POINT('',#45255);
#16492=EDGE_CURVE('',#13083,#13083,#10772,.T.);
#16493=EDGE_CURVE('',#13084,#13084,#10773,.T.);
#16494=EDGE_CURVE('',#13084,#13083,#3335,.T.);
#16495=EDGE_CURVE('',#13085,#13085,#10774,.T.);
#16496=EDGE_CURVE('',#13085,#13084,#3336,.T.);
#16497=EDGE_CURVE('',#13086,#13086,#10775,.T.);
#16498=EDGE_CURVE('',#13086,#13085,#3337,.T.);
#22976=ORIENTED_EDGE('',*,*,#16492,.F.);
#22977=ORIENTED_EDGE('',*,*,#16493,.F.);
#22978=ORIENTED_EDGE('',*,*,#16494,.T.);
#22979=ORIENTED_EDGE('',*,*,#16492,.T.);
#22980=ORIENTED_EDGE('',*,*,#16494,.F.);
#22981=ORIENTED_EDGE('',*,*,#16495,.F.);
#22982=ORIENTED_EDGE('',*,*,#16496,.T.);
#22983=ORIENTED_EDGE('',*,*,#16493,.T.);
#22984=ORIENTED_EDGE('',*,*,#16496,.F.);
#22985=ORIENTED_EDGE('',*,*,#16497,.F.);
#22986=ORIENTED_EDGE('',*,*,#16498,.T.);
#22987=ORIENTED_EDGE('',*,*,#16495,.T.);
#22988=ORIENTED_EDGE('',*,*,#16498,.F.);
#22989=ORIENTED_EDGE('',*,*,#16497,.T.);
#26670=ADVANCED_FACE('',(#7846),#1393,.T.);
#26671=ADVANCED_FACE('',(#7847),#377,.T.);
#26672=ADVANCED_FACE('',(#7848),#6691,.T.);
#26673=ADVANCED_FACE('',(#7849),#378,.T.);
#26674=ADVANCED_FACE('',(#7850),#1394,.T.);
#27229=CLOSED_SHELL('',(#26670,#26671,#26672,#26673,#26674));
#29177=AXIS2_PLACEMENT_3D('',#45242,#34983,#34984);
#29178=AXIS2_PLACEMENT_3D('',#45243,#34985,#34986);
#29179=AXIS2_PLACEMENT_3D('',#45245,#34987,#34988);
#29180=AXIS2_PLACEMENT_3D('',#45246,#34989,#34990);
#29181=AXIS2_PLACEMENT_3D('',#45248,#34991,#34992);
#29182=AXIS2_PLACEMENT_3D('',#45250,#34994,#34995);
#29183=AXIS2_PLACEMENT_3D('',#45252,#34996,#34997);
#29184=AXIS2_PLACEMENT_3D('',#45254,#34999,#35000);
#29185=AXIS2_PLACEMENT_3D('',#45256,#35001,#35002);
#29186=AXIS2_PLACEMENT_3D('',#45258,#35004,#35005);
#34983=DIRECTION('axis',(0.,0.,1.));
#34984=DIRECTION('refdir',(1.,0.,0.));
#34985=DIRECTION('center_axis',(-1.,0.,0.));
#34986=DIRECTION('ref_axis',(0.,0.,1.));
#34987=DIRECTION('center_axis',(1.,0.,0.));
#34988=DIRECTION('ref_axis',(0.,0.,-1.));
#34989=DIRECTION('center_axis',(1.,0.,0.));
#34990=DIRECTION('ref_axis',(0.,1.,0.));
#34991=DIRECTION('center_axis',(1.,0.,0.));
#34992=DIRECTION('ref_axis',(0.,0.,-1.));
#34993=DIRECTION('',(-0.707106781186548,0.707106781186547,8.65956056235493E-17));
#34994=DIRECTION('center_axis',(1.,0.,0.));
#34995=DIRECTION('ref_axis',(0.,1.,0.));
#34996=DIRECTION('center_axis',(1.,0.,0.));
#34997=DIRECTION('ref_axis',(0.,0.,-1.));
#34998=DIRECTION('',(-1.,0.,0.));
#34999=DIRECTION('center_axis',(-1.,0.,0.));
#35000=DIRECTION('ref_axis',(0.,1.,0.));
#35001=DIRECTION('center_axis',(1.,0.,0.));
#35002=DIRECTION('ref_axis',(0.,0.,-1.));
#35003=DIRECTION('',(-0.707106781186548,-0.707106781186547,-8.65956056235493E-17));
#35004=DIRECTION('center_axis',(1.,0.,0.));
#35005=DIRECTION('ref_axis',(0.,0.,-1.));
#45242=CARTESIAN_POINT('',(0.,0.,0.));
#45243=CARTESIAN_POINT('Origin',(-11.5,2.2,0.));
#45244=CARTESIAN_POINT('',(-11.5,-2.2,-2.69422295812418E-16));
#45245=CARTESIAN_POINT('Origin',(-11.5,0.,0.));
#45246=CARTESIAN_POINT('Origin',(-11.35,0.,0.));
#45247=CARTESIAN_POINT('',(-11.2,-2.5,-3.06161699786838E-16));
#45248=CARTESIAN_POINT('Origin',(-11.2,0.,0.));
#45249=CARTESIAN_POINT('',(-11.35,-2.35,-2.87791997799628E-16));
#45250=CARTESIAN_POINT('Origin',(0.,0.,0.));
#45251=CARTESIAN_POINT('',(11.2,-2.5,-3.06161699786838E-16));
#45252=CARTESIAN_POINT('Origin',(11.2,0.,0.));
#45253=CARTESIAN_POINT('',(0.,-2.5,-3.06161699786838E-16));
#45254=CARTESIAN_POINT('Origin',(11.35,0.,0.));
#45255=CARTESIAN_POINT('',(11.5,-2.2,-2.69422295812418E-16));
#45256=CARTESIAN_POINT('Origin',(11.5,0.,0.));
#45257=CARTESIAN_POINT('',(11.35,-2.35,-2.87791997799628E-16));
#45258=CARTESIAN_POINT('Origin',(11.5,0.,0.));
#55703=UNCERTAINTY_MEASURE_WITH_UNIT(LENGTH_MEASURE(0.01),#55738,
'DISTANCE_ACCURACY_VALUE',
'Maximum model space distance between geometric entities at asserted c
onnectivities');
#55715=UNCERTAINTY_MEASURE_WITH_UNIT(LENGTH_MEASURE(0.01),#55738,
'DISTANCE_ACCURACY_VALUE',
'Maximum model space distance between geometric entities at asserted c
onnectivities');
#55725=(
GEOMETRIC_REPRESENTATION_CONTEXT(3)
GLOBAL_UNCERTAINTY_ASSIGNED_CONTEXT((#55703))
GLOBAL_UNIT_ASSIGNED_CONTEXT((#55738,#55740,#55741))
REPRESENTATION_CONTEXT('','3D')
);
#55737=(
GEOMETRIC_REPRESENTATION_CONTEXT(3)
GLOBAL_UNCERTAINTY_ASSIGNED_CONTEXT((#55715))
GLOBAL_UNIT_ASSIGNED_CONTEXT((#55738,#55740,#55741))
REPRESENTATION_CONTEXT('','3D')
);
#55738=(
LENGTH_UNIT()
NAMED_UNIT(*)
SI_UNIT(.MILLI.,.METRE.)
);
#55740=(
NAMED_UNIT(*)
PLANE_ANGLE_UNIT()
SI_UNIT($,.RADIAN.)
);
#55741=(
NAMED_UNIT(*)
SI_UNIT($,.STERADIAN.)
SOLID_ANGLE_UNIT()
);
#55751=SHAPE_DEFINITION_REPRESENTATION(#55772,#55829);
#55772=PRODUCT_DEFINITION_SHAPE('',$,#55851);
#55829=SHAPE_REPRESENTATION('',(#29177),#55725);
#55841=PRODUCT_DEFINITION_CONTEXT('part definition',#55906,'design');
#55851=PRODUCT_DEFINITION('2026-10-26-00-34-25-074',
'09_Impeller_Drive_Pin_D5x23',#55872,#55841);
#55872=PRODUCT_DEFINITION_FORMATION('',$,#55917);
#55906=APPLICATION_CONTEXT(
'Core Data for Automotive Mechanical Design Process');
#55907=PRODUCT_CONTEXT('part definition',#55906,'mechanical');
#55917=PRODUCT('2026-10-26-00-34-25-074','09_Impeller_Drive_Pin_D5x23',
$,(#55907));
#55985=COLOUR_RGB('Grey',0.48,0.52,0.57);
#55986=FILL_AREA_STYLE_COLOUR('',#55985);
#55987=FILL_AREA_STYLE('',(#55986));
#55988=SURFACE_STYLE_FILL_AREA(#55987);
#55989=SURFACE_SIDE_STYLE('',(#55988));
#55990=SURFACE_STYLE_USAGE(.BOTH.,#55989);
#55991=PRESENTATION_STYLE_ASSIGNMENT((#55990));
ENDSEC;
END-ISO-10303-21;
